ISO-10303-21;
HEADER;
/* Generated by software containing ST-Developer
 * from STEP Tools, Inc. (www.steptools.com) 
 */

FILE_DESCRIPTION(
/* description */ ('Jaw-coupled motor to shaft test stand'),
/* implementation_level */ '2;1');

FILE_NAME(
/* name */ 'M3x10 motor screw.step',
/* time_stamp */ '2026-10-27T10:46:06-07:00',
/* author */ (''),
/* organization */ (''),
/* preprocessor_version */ 'ST-DEVELOPER v20.2',
/* originating_system */ 'Autodesk Translation Framework v15.17.0.0',
/* authorisation */ '');

FILE_SCHEMA (('AUTOMOTIVE_DESIGN { 1 0 10303 214 3 1 1 }'));
ENDSEC;

DATA;
#10=MECHANICAL_DESIGN_GEOMETRIC_PRESENTATION_REPRESENTATION('',(#349),#19361);
#285=SHAPE_REPRESENTATION_RELATIONSHIP('SRR','None',#19499,#317);
#317=ADVANCED_BREP_SHAPE_REPRESENTATION('',(#382),#19335);
#349=STYLED_ITEM('',(#19753),#382);
#382=MANIFOLD_SOLID_BREP('Body1',#10993);
#444=FACE_BOUND('',#1763,.T.);
#445=FACE_BOUND('',#1766,.T.);
#561=PLANE('',#11511);
#562=PLANE('',#11512);
#563=PLANE('',#11513);
#564=PLANE('',#11514);
#565=PLANE('',#11515);
#566=PLANE('',#11516);
#567=PLANE('',#11517);
#568=PLANE('',#11518);
#569=PLANE('',#11523);
#570=PLANE('',#11526);
#1094=FACE_OUTER_BOUND('',#1755,.T.);
#1095=FACE_OUTER_BOUND('',#1756,.T.);
#1096=FACE_OUTER_BOUND('',#1757,.T.);
#1097=FACE_OUTER_BOUND('',#1758,.T.);
#1098=FACE_OUTER_BOUND('',#1759,.T.);
#1099=FACE_OUTER_BOUND('',#1760,.T.);
#1100=FACE_OUTER_BOUND('',#1761,.T.);
#1101=FACE_OUTER_BOUND('',#1762,.T.);
#1102=FACE_OUTER_BOUND('',#1764,.T.);
#1103=FACE_OUTER_BOUND('',#1765,.T.);
#1104=FACE_OUTER_BOUND('',#1767,.T.);
#1105=FACE_OUTER_BOUND('',#1768,.T.);
#1755=EDGE_LOOP('',(#7640,#7641,#7642,#7643));
#1756=EDGE_LOOP('',(#7644,#7645,#7646,#7647));
#1757=EDGE_LOOP('',(#7648,#7649,#7650,#7651));
#1758=EDGE_LOOP('',(#7652,#7653,#7654,#7655));
#1759=EDGE_LOOP('',(#7656,#7657,#7658,#7659));
#1760=EDGE_LOOP('',(#7660,#7661,#7662,#7663));
#1761=EDGE_LOOP('',(#7664,#7665,#7666,#7667,#7668,#7669));
#1762=EDGE_LOOP('',(#7670));
#1763=EDGE_LOOP('',(#7671));
#1764=EDGE_LOOP('',(#7672,#7673,#7674,#7675));
#1765=EDGE_LOOP('',(#7676));
#1766=EDGE_LOOP('',(#7677,#7678,#7679,#7680,#7681,#7682));
#1767=EDGE_LOOP('',(#7683,#7684,#7685,#7686));
#1768=EDGE_LOOP('',(#7687));
#2468=LINE('',#15759,#3621);
#2469=LINE('',#15761,#3622);
#2470=LINE('',#15763,#3623);
#2471=LINE('',#15764,#3624);
#2472=LINE('',#15767,#3625);
#2473=LINE('',#15769,#3626);
#2474=LINE('',#15770,#3627);
#2475=LINE('',#15773,#3628);
#2476=LINE('',#15775,#3629);
#2477=LINE('',#15776,#3630);
#2478=LINE('',#15779,#3631);
#2479=LINE('',#15781,#3632);
#2480=LINE('',#15782,#3633);
#2481=LINE('',#15785,#3634);
#2482=LINE('',#15787,#3635);
#2483=LINE('',#15788,#3636);
#2484=LINE('',#15790,#3637);
#2485=LINE('',#15791,#3638);
#2486=LINE('',#15801,#3639);
#2487=LINE('',#15805,#3640);
#3621=VECTOR('',#12711,1.);
#3622=VECTOR('',#12712,1.);
#3623=VECTOR('',#12713,1.);
#3624=VECTOR('',#12714,1.);
#3625=VECTOR('',#12717,1.);
#3626=VECTOR('',#12718,1.);
#3627=VECTOR('',#12719,1.);
#3628=VECTOR('',#12722,1.);
#3629=VECTOR('',#12723,1.);
#3630=VECTOR('',#12724,1.);
#3631=VECTOR('',#12727,1.);
#3632=VECTOR('',#12728,1.);
#3633=VECTOR('',#12729,1.);
#3634=VECTOR('',#12732,1.);
#3635=VECTOR('',#12733,1.);
#3636=VECTOR('',#12734,1.);
#3637=VECTOR('',#12737,1.);
#3638=VECTOR('',#12738,1.);
#3639=VECTOR('',#12751,0.275);
#3640=VECTOR('',#12756,0.15);
#4735=CIRCLE('',#11519,0.275);
#4736=CIRCLE('',#11520,0.15);
#4737=CIRCLE('',#11522,0.275);
#4738=CIRCLE('',#11525,0.15);
#5041=VERTEX_POINT('',#15757);
#5042=VERTEX_POINT('',#15758);
#5043=VERTEX_POINT('',#15760);
#5044=VERTEX_POINT('',#15762);
#5045=VERTEX_POINT('',#15766);
#5046=VERTEX_POINT('',#15768);
#5047=VERTEX_POINT('',#15772);
#5048=VERTEX_POINT('',#15774);
#5049=VERTEX_POINT('',#15778);
#5050=VERTEX_POINT('',#15780);
#5051=VERTEX_POINT('',#15784);
#5052=VERTEX_POINT('',#15786);
#5053=VERTEX_POINT('',#15794);
#5054=VERTEX_POINT('',#15796);
#5055=VERTEX_POINT('',#15799);
#5056=VERTEX_POINT('',#15804);
#6031=EDGE_CURVE('',#5041,#5042,#2468,.T.);
#6032=EDGE_CURVE('',#5043,#5041,#2469,.T.);
#6033=EDGE_CURVE('',#5043,#5044,#2470,.T.);
#6034=EDGE_CURVE('',#5044,#5042,#2471,.T.);
#6035=EDGE_CURVE('',#5042,#5045,#2472,.T.);
#6036=EDGE_CURVE('',#5044,#5046,#2473,.T.);
#6037=EDGE_CURVE('',#5046,#5045,#2474,.T.);
#6038=EDGE_CURVE('',#5045,#5047,#2475,.T.);
#6039=EDGE_CURVE('',#5046,#5048,#2476,.T.);
#6040=EDGE_CURVE('',#5048,#5047,#2477,.T.);
#6041=EDGE_CURVE('',#5047,#5049,#2478,.T.);
#6042=EDGE_CURVE('',#5048,#5050,#2479,.T.);
#6043=EDGE_CURVE('',#5050,#5049,#2480,.T.);
#6044=EDGE_CURVE('',#5049,#5051,#2481,.T.);
#6045=EDGE_CURVE('',#5050,#5052,#2482,.T.);
#6046=EDGE_CURVE('',#5052,#5051,#2483,.T.);
#6047=EDGE_CURVE('',#5051,#5041,#2484,.T.);
#6048=EDGE_CURVE('',#5052,#5043,#2485,.T.);
#6049=EDGE_CURVE('',#5053,#5053,#4735,.T.);
#6050=EDGE_CURVE('',#5054,#5054,#4736,.T.);
#6051=EDGE_CURVE('',#5055,#5055,#4737,.T.);
#6052=EDGE_CURVE('',#5055,#5053,#2486,.T.);
#6053=EDGE_CURVE('',#5054,#5056,#2487,.T.);
#6054=EDGE_CURVE('',#5056,#5056,#4738,.T.);
#7640=ORIENTED_EDGE('',*,*,#6031,.F.);
#7641=ORIENTED_EDGE('',*,*,#6032,.F.);
#7642=ORIENTED_EDGE('',*,*,#6033,.T.);
#7643=ORIENTED_EDGE('',*,*,#6034,.T.);
#7644=ORIENTED_EDGE('',*,*,#6035,.F.);
#7645=ORIENTED_EDGE('',*,*,#6034,.F.);
#7646=ORIENTED_EDGE('',*,*,#6036,.T.);
#7647=ORIENTED_EDGE('',*,*,#6037,.T.);
#7648=ORIENTED_EDGE('',*,*,#6038,.F.);
#7649=ORIENTED_EDGE('',*,*,#6037,.F.);
#7650=ORIENTED_EDGE('',*,*,#6039,.T.);
#7651=ORIENTED_EDGE('',*,*,#6040,.T.);
#7652=ORIENTED_EDGE('',*,*,#6041,.F.);
#7653=ORIENTED_EDGE('',*,*,#6040,.F.);
#7654=ORIENTED_EDGE('',*,*,#6042,.T.);
#7655=ORIENTED_EDGE('',*,*,#6043,.T.);
#7656=ORIENTED_EDGE('',*,*,#6044,.F.);
#7657=ORIENTED_EDGE('',*,*,#6043,.F.);
#7658=ORIENTED_EDGE('',*,*,#6045,.T.);
#7659=ORIENTED_EDGE('',*,*,#6046,.T.);
#7660=ORIENTED_EDGE('',*,*,#6047,.F.);
#7661=ORIENTED_EDGE('',*,*,#6046,.F.);
#7662=ORIENTED_EDGE('',*,*,#6048,.T.);
#7663=ORIENTED_EDGE('',*,*,#6032,.T.);
#7664=ORIENTED_EDGE('',*,*,#6039,.F.);
#7665=ORIENTED_EDGE('',*,*,#6036,.F.);
#7666=ORIENTED_EDGE('',*,*,#6033,.F.);
#7667=ORIENTED_EDGE('',*,*,#6048,.F.);
#7668=ORIENTED_EDGE('',*,*,#6045,.F.);
#7669=ORIENTED_EDGE('',*,*,#6042,.F.);
#7670=ORIENTED_EDGE('',*,*,#6049,.F.);
#7671=ORIENTED_EDGE('',*,*,#6050,.T.);
#7672=ORIENTED_EDGE('',*,*,#6051,.F.);
#7673=ORIENTED_EDGE('',*,*,#6052,.T.);
#7674=ORIENTED_EDGE('',*,*,#6049,.T.);
#7675=ORIENTED_EDGE('',*,*,#6052,.F.);
#7676=ORIENTED_EDGE('',*,*,#6051,.T.);
#7677=ORIENTED_EDGE('',*,*,#6041,.T.);
#7678=ORIENTED_EDGE('',*,*,#6044,.T.);
#7679=ORIENTED_EDGE('',*,*,#6047,.T.);
#7680=ORIENTED_EDGE('',*,*,#6031,.T.);
#7681=ORIENTED_EDGE('',*,*,#6035,.T.);
#7682=ORIENTED_EDGE('',*,*,#6038,.T.);
#7683=ORIENTED_EDGE('',*,*,#6050,.F.);
#7684=ORIENTED_EDGE('',*,*,#6053,.T.);
#7685=ORIENTED_EDGE('',*,*,#6054,.T.);
#7686=ORIENTED_EDGE('',*,*,#6053,.F.);
#7687=ORIENTED_EDGE('',*,*,#6054,.F.);
#10297=CYLINDRICAL_SURFACE('',#11521,0.275);
#10298=CYLINDRICAL_SURFACE('',#11524,0.15);
#10436=ADVANCED_FACE('',(#1094),#561,.F.);
#10437=ADVANCED_FACE('',(#1095),#562,.F.);
#10438=ADVANCED_FACE('',(#1096),#563,.F.);
#10439=ADVANCED_FACE('',(#1097),#564,.F.);
#10440=ADVANCED_FACE('',(#1098),#565,.F.);
#10441=ADVANCED_FACE('',(#1099),#566,.F.);
#10442=ADVANCED_FACE('',(#1100),#567,.T.);
#10443=ADVANCED_FACE('',(#1101,#444),#568,.F.);
#10444=ADVANCED_FACE('',(#1102),#10297,.T.);
#10445=ADVANCED_FACE('',(#1103,#445),#569,.T.);
#10446=ADVANCED_FACE('',(#1104),#10298,.T.);
#10447=ADVANCED_FACE('',(#1105),#570,.F.);
#10993=CLOSED_SHELL('',(#10436,#10437,#10438,#10439,#10440,#10441,#10442,
#10443,#10444,#10445,#10446,#10447));
#11510=AXIS2_PLACEMENT_3D('',#15755,#12707,#12708);
#11511=AXIS2_PLACEMENT_3D('',#15756,#12709,#12710);
#11512=AXIS2_PLACEMENT_3D('',#15765,#12715,#12716);
#11513=AXIS2_PLACEMENT_3D('',#15771,#12720,#12721);
#11514=AXIS2_PLACEMENT_3D('',#15777,#12725,#12726);
#11515=AXIS2_PLACEMENT_3D('',#15783,#12730,#12731);
#11516=AXIS2_PLACEMENT_3D('',#15789,#12735,#12736);
#11517=AXIS2_PLACEMENT_3D('',#15792,#12739,#12740);
#11518=AXIS2_PLACEMENT_3D('',#15793,#12741,#12742);
#11519=AXIS2_PLACEMENT_3D('',#15795,#12743,#12744);
#11520=AXIS2_PLACEMENT_3D('',#15797,#12745,#12746);
#11521=AXIS2_PLACEMENT_3D('',#15798,#12747,#12748);
#11522=AXIS2_PLACEMENT_3D('',#15800,#12749,#12750);
#11523=AXIS2_PLACEMENT_3D('',#15802,#12752,#12753);
#11524=AXIS2_PLACEMENT_3D('',#15803,#12754,#12755);
#11525=AXIS2_PLACEMENT_3D('',#15806,#12757,#12758);
#11526=AXIS2_PLACEMENT_3D('',#15807,#12759,#12760);
#12707=DIRECTION('axis',(0.,0.,1.));
#12708=DIRECTION('refdir',(1.,0.,0.));
#12709=DIRECTION('center_axis',(-0.866025403784438,0.,0.5));
#12710=DIRECTION('ref_axis',(0.5,0.,0.866025403784438));
#12711=DIRECTION('',(-0.5,0.,-0.866025403784438));
#12712=DIRECTION('',(0.,1.,0.));
#12713=DIRECTION('',(-0.5,0.,-0.866025403784438));
#12714=DIRECTION('',(0.,1.,0.));
#12715=DIRECTION('center_axis',(-0.866025403784438,0.,-0.5));
#12716=DIRECTION('ref_axis',(-0.5,0.,0.866025403784438));
#12717=DIRECTION('',(0.5,0.,-0.866025403784438));
#12718=DIRECTION('',(0.5,0.,-0.866025403784438));
#12719=DIRECTION('',(0.,1.,0.));
#12720=DIRECTION('center_axis',(0.,0.,-1.));
#12721=DIRECTION('ref_axis',(-1.,0.,0.));
#12722=DIRECTION('',(1.,0.,0.));
#12723=DIRECTION('',(1.,0.,0.));
#12724=DIRECTION('',(0.,1.,0.));
#12725=DIRECTION('center_axis',(0.866025403784439,0.,-0.499999999999999));
#12726=DIRECTION('ref_axis',(-0.499999999999999,0.,-0.866025403784439));
#12727=DIRECTION('',(0.499999999999999,0.,0.866025403784439));
#12728=DIRECTION('',(0.499999999999999,0.,0.866025403784439));
#12729=DIRECTION('',(0.,1.,0.));
#12730=DIRECTION('center_axis',(0.866025403784439,0.,0.499999999999999));
#12731=DIRECTION('ref_axis',(0.499999999999999,0.,-0.866025403784439));
#12732=DIRECTION('',(-0.499999999999999,0.,0.866025403784439));
#12733=DIRECTION('',(-0.499999999999999,0.,0.866025403784439));
#12734=DIRECTION('',(0.,1.,0.));
#12735=DIRECTION('center_axis',(0.,0.,1.));
#12736=DIRECTION('ref_axis',(1.,0.,0.));
#12737=DIRECTION('',(-1.,0.,0.));
#12738=DIRECTION('',(-1.,0.,0.));
#12739=DIRECTION('center_axis',(0.,1.,0.));
#12740=DIRECTION('ref_axis',(1.,0.,0.));
#12741=DIRECTION('center_axis',(0.,1.,0.));
#12742=DIRECTION('ref_axis',(1.,0.,0.));
#12743=DIRECTION('center_axis',(0.,1.,0.));
#12744=DIRECTION('ref_axis',(1.,0.,0.));
#12745=DIRECTION('center_axis',(0.,1.,0.));
#12746=DIRECTION('ref_axis',(1.,0.,0.));
#12747=DIRECTION('center_axis',(0.,1.,0.));
#12748=DIRECTION('ref_axis',(1.,0.,0.));
#12749=DIRECTION('center_axis',(0.,1.,0.));
#12750=DIRECTION('ref_axis',(1.,0.,0.));
#12751=DIRECTION('',(0.,-1.,0.));
#12752=DIRECTION('center_axis',(0.,1.,0.));
#12753=DIRECTION('ref_axis',(1.,0.,0.));
#12754=DIRECTION('center_axis',(0.,1.,0.));
#12755=DIRECTION('ref_axis',(1.,0.,0.));
#12756=DIRECTION('',(0.,-1.,0.));
#12757=DIRECTION('center_axis',(0.,1.,0.));
#12758=DIRECTION('ref_axis',(1.,0.,0.));
#12759=DIRECTION('center_axis',(0.,1.,0.));
#12760=DIRECTION('ref_axis',(1.,0.,0.));
#15755=CARTESIAN_POINT('',(0.,0.,0.));
#15756=CARTESIAN_POINT('Origin',(-1.69433756729741,-6.9,2.67));
#15757=CARTESIAN_POINT('',(-1.6221687836487,-6.7,2.795));
#15758=CARTESIAN_POINT('',(-1.69433756729741,-6.7,2.67));
#15759=CARTESIAN_POINT('',(-1.67629537138523,-6.7,2.70125));
#15760=CARTESIAN_POINT('',(-1.6221687836487,-6.9,2.795));
#15761=CARTESIAN_POINT('',(-1.6221687836487,-6.9,2.795));
#15762=CARTESIAN_POINT('',(-1.69433756729741,-6.9,2.67));
#15763=CARTESIAN_POINT('',(-1.6221687836487,-6.9,2.795));
#15764=CARTESIAN_POINT('',(-1.69433756729741,-6.9,2.67));
#15765=CARTESIAN_POINT('Origin',(-1.6221687836487,-6.9,2.545));
#15766=CARTESIAN_POINT('',(-1.6221687836487,-6.7,2.545));
#15767=CARTESIAN_POINT('',(-1.64021097956088,-6.7,2.57625));
#15768=CARTESIAN_POINT('',(-1.6221687836487,-6.9,2.545));
#15769=CARTESIAN_POINT('',(-1.69433756729741,-6.9,2.67));
#15770=CARTESIAN_POINT('',(-1.6221687836487,-6.9,2.545));
#15771=CARTESIAN_POINT('Origin',(-1.4778312163513,-6.9,2.545));
#15772=CARTESIAN_POINT('',(-1.4778312163513,-6.7,2.545));
#15773=CARTESIAN_POINT('',(-1.51391560817565,-6.7,2.545));
#15774=CARTESIAN_POINT('',(-1.4778312163513,-6.9,2.545));
#15775=CARTESIAN_POINT('',(-1.6221687836487,-6.9,2.545));
#15776=CARTESIAN_POINT('',(-1.4778312163513,-6.9,2.545));
#15777=CARTESIAN_POINT('Origin',(-1.40566243270259,-6.9,2.67));
#15778=CARTESIAN_POINT('',(-1.40566243270259,-6.7,2.67));
#15779=CARTESIAN_POINT('',(-1.42370462861477,-6.7,2.63875));
#15780=CARTESIAN_POINT('',(-1.40566243270259,-6.9,2.67));
#15781=CARTESIAN_POINT('',(-1.4778312163513,-6.9,2.545));
#15782=CARTESIAN_POINT('',(-1.40566243270259,-6.9,2.67));
#15783=CARTESIAN_POINT('Origin',(-1.4778312163513,-6.9,2.795));
#15784=CARTESIAN_POINT('',(-1.4778312163513,-6.7,2.795));
#15785=CARTESIAN_POINT('',(-1.45978902043912,-6.7,2.76375));
#15786=CARTESIAN_POINT('',(-1.4778312163513,-6.9,2.795));
#15787=CARTESIAN_POINT('',(-1.40566243270259,-6.9,2.67));
#15788=CARTESIAN_POINT('',(-1.4778312163513,-6.9,2.795));
#15789=CARTESIAN_POINT('Origin',(-1.6221687836487,-6.9,2.795));
#15790=CARTESIAN_POINT('',(-1.58608439182435,-6.7,2.795));
#15791=CARTESIAN_POINT('',(-1.4778312163513,-6.9,2.795));
#15792=CARTESIAN_POINT('Origin',(-1.55,-6.9,2.67));
#15793=CARTESIAN_POINT('Origin',(-1.55,-7.,2.67));
#15794=CARTESIAN_POINT('',(-1.825,-7.,2.67));
#15795=CARTESIAN_POINT('Origin',(-1.55,-7.,2.67));
#15796=CARTESIAN_POINT('',(-1.7,-7.,2.67));
#15797=CARTESIAN_POINT('Origin',(-1.55,-7.,2.67));
#15798=CARTESIAN_POINT('Origin',(-1.55,-7.,2.67));
#15799=CARTESIAN_POINT('',(-1.825,-6.7,2.67));
#15800=CARTESIAN_POINT('Origin',(-1.55,-6.7,2.67));
#15801=CARTESIAN_POINT('',(-1.825,-7.,2.67));
#15802=CARTESIAN_POINT('Origin',(-1.55,-6.7,2.67));
#15803=CARTESIAN_POINT('Origin',(-1.55,-8.,2.67));
#15804=CARTESIAN_POINT('',(-1.7,-8.,2.67));
#15805=CARTESIAN_POINT('',(-1.7,-8.,2.67));
#15806=CARTESIAN_POINT('Origin',(-1.55,-8.,2.67));
#15807=CARTESIAN_POINT('Origin',(-1.55,-8.,2.67));
#19297=UNCERTAINTY_MEASURE_WITH_UNIT(LENGTH_MEASURE(0.001),#19362,
'DISTANCE_ACCURACY_VALUE',
'Maximum model space distance between geometric entities at asserted c
onnectivities');
#19323=UNCERTAINTY_MEASURE_WITH_UNIT(LENGTH_MEASURE(0.001),#19362,
'DISTANCE_ACCURACY_VALUE',
'Maximum model space distance between geometric entities at asserted c
onnectivities');
#19335=(
GEOMETRIC_REPRESENTATION_CONTEXT(3)
GLOBAL_UNCERTAINTY_ASSIGNED_CONTEXT((#19297))
GLOBAL_UNIT_ASSIGNED_CONTEXT((#19362,#19364,#19365))
REPRESENTATION_CONTEXT('','3D')
);
#19361=(
GEOMETRIC_REPRESENTATION_CONTEXT(3)
GLOBAL_UNCERTAINTY_ASSIGNED_CONTEXT((#19323))
GLOBAL_UNIT_ASSIGNED_CONTEXT((#19362,#19364,#19365))
REPRESENTATION_CONTEXT('','3D')
);
#19362=(
LENGTH_UNIT()
NAMED_UNIT(*)
SI_UNIT(.CENTI.,.METRE.)
);
#19364=(
NAMED_UNIT(*)
PLANE_ANGLE_UNIT()
SI_UNIT($,.RADIAN.)
);
#19365=(
NAMED_UNIT(*)
SI_UNIT($,.STERADIAN.)
SOLID_ANGLE_UNIT()
);
#19377=SHAPE_DEFINITION_REPRESENTATION(#19414,#19499);
#19414=PRODUCT_DEFINITION_SHAPE('',$,#19537);
#19499=SHAPE_REPRESENTATION('',(#11510),#19335);
#19525=PRODUCT_DEFINITION_CONTEXT('part definition',#19638,'design');
#19537=PRODUCT_DEFINITION('M3x10 motor screw','M3x10 motor screw',#19574,
#19525);
#19574=PRODUCT_DEFINITION_FORMATION('',$,#19651);
#19638=APPLICATION_CONTEXT(
'Core Data for Automotive Mechanical Design Process');
#19639=PRODUCT_CONTEXT('part definition',#19638,'mechanical');
#19651=PRODUCT('M3x10 motor screw','M3x10 motor screw',
'M3x10 motor screw',(#19639));
#19747=COLOUR_RGB('Black',0.12,0.14,0.17);
#19748=FILL_AREA_STYLE_COLOUR('',#19747);
#19749=FILL_AREA_STYLE('',(#19748));
#19750=SURFACE_STYLE_FILL_AREA(#19749);
#19751=SURFACE_SIDE_STYLE('',(#19750));
#19752=SURFACE_STYLE_USAGE(.BOTH.,#19751);
#19753=PRESENTATION_STYLE_ASSIGNMENT((#19752));
ENDSEC;
END-ISO-10303-21;
